ISO-10303-21;
HEADER;
FILE_DESCRIPTION (('STEP AP214'),
    '1' );
FILE_NAME ('Housing Seal.step',
    '2026-10-22T18:53:08',
    ( '' ),
    ( '' ),
    'SwSTEP 2.0',
    'SolidWorks 2025',
    '' );
FILE_SCHEMA (( 'AUTOMOTIVE_DESIGN' ));
ENDSEC;

DATA;
#54=CARTESIAN_POINT ( 'NONE',  ( 20.85000000000000497, -15.04000000000000092, 2.200000000000000178 ) ) ;
#165=CYLINDRICAL_SURFACE ( 'NONE', #16449, 23.85000000000000142 ) ;
#211=DIRECTION ( 'NONE',  ( 0.000000000000000000, 0.000000000000000000, 1.000000000000000000 ) ) ;
#258=PLANE ( 'NONE',  #10310 ) ;
#364=EDGE_LOOP ( 'NONE', ( #5051, #10753, #2893, #23678 ) ) ;
#369=DIRECTION ( 'NONE',  ( 1.000000000000000000, 0.000000000000000000, -0.000000000000000000 ) ) ;
#474=CARTESIAN_POINT ( 'NONE',  ( 23.85000000000000142, -15.03999999999999737, 2.200000000000000178 ) ) ;
#515=AXIS2_PLACEMENT_3D ( 'NONE', #20081, #16040, #23502 ) ;
#530=VERTEX_POINT ( 'NONE', #17315 ) ;
#637=( NAMED_UNIT ( * ) SI_UNIT ( $, .STERADIAN. ) SOLID_ANGLE_UNIT ( ) );
#751=( LENGTH_UNIT ( ) NAMED_UNIT ( * ) SI_UNIT ( .MILLI., .METRE. ) );
#885=AXIS2_PLACEMENT_3D ( 'NONE', #18229, #8575, #17984 ) ;
#957=LINE ( 'NONE', #14005, #19246 ) ;
#1179=PLANE ( 'NONE',  #515 ) ;
#1202=ADVANCED_FACE ( 'NONE', ( #19406 ), #1224, .F. ) ;
#1224=PLANE ( 'NONE',  #13343 ) ;
#1289=EDGE_CURVE ( 'NONE', #14785, #19122, #19106, .T. ) ;
#1303=CARTESIAN_POINT ( 'NONE',  ( 0.000000000000000000, 15.03999999999999737, 0.000000000000000000 ) ) ;
#1331=ORIENTED_EDGE ( 'NONE', *, *, #22070, .F. ) ;
#1438=ADVANCED_FACE ( 'NONE', ( #19945 ), #19840, .F. ) ;
#1456=CYLINDRICAL_SURFACE ( 'NONE', #4397, 23.85000000000000142 ) ;
#1679=AXIS2_PLACEMENT_3D ( 'NONE', #16031, #7947, #15257 ) ;
#1825=DIRECTION ( 'NONE',  ( 1.000000000000000000, 0.000000000000000000, 0.000000000000000000 ) ) ;
#1838=CIRCLE ( 'NONE', #12725, 20.85000000000000497 ) ;
#1907=DIRECTION ( 'NONE',  ( -1.000000000000000000, 0.000000000000000000, 0.000000000000000000 ) ) ;
#2118=ORIENTED_EDGE ( 'NONE', *, *, #2550, .T. ) ;
#2159=MANIFOLD_SOLID_BREP ( 'Boss-Extrude1', #16698 ) ;
#2202=PRODUCT_DEFINITION_FORMATION_WITH_SPECIFIED_SOURCE ( 'ANY', '', #9355, .NOT_KNOWN. ) ;
#2302=ORIENTED_EDGE ( 'NONE', *, *, #2550, .F. ) ;
#2348=EDGE_CURVE ( 'NONE', #530, #9521, #13021, .T. ) ;
#2492=EDGE_CURVE ( 'NONE', #4092, #19904, #15180, .T. ) ;
#2550=EDGE_CURVE ( 'NONE', #21161, #21353, #17033, .T. ) ;
#2565=VERTEX_POINT ( 'NONE', #5816 ) ;
#2566=AXIS2_PLACEMENT_3D ( 'NONE', #23828, #5410, #7108 ) ;
#2613=ORIENTED_EDGE ( 'NONE', *, *, #22070, .T. ) ;
#2681=( NAMED_UNIT ( * ) PLANE_ANGLE_UNIT ( ) SI_UNIT ( $, .RADIAN. ) );
#2893=ORIENTED_EDGE ( 'NONE', *, *, #4035, .T. ) ;
#2985=CIRCLE ( 'NONE', #8818, 23.85000000000000142 ) ;
#2986=CARTESIAN_POINT ( 'NONE',  ( -20.85000000000000497, 15.03999999999999915, 2.200000000000000178 ) ) ;
#3024=PRODUCT_DEFINITION_SHAPE ( 'NONE', 'NONE',  #13774 ) ;
#3033=UNCERTAINTY_MEASURE_WITH_UNIT (LENGTH_MEASURE( 1.000000000000000082E-05 ), #751, 'distance_accuracy_value', 'NONE');
#3098=CYLINDRICAL_SURFACE ( 'NONE', #885, 20.85000000000000497 ) ;
#3168=CARTESIAN_POINT ( 'NONE',  ( 0.000000000000000000, -15.03999999999999737, 0.000000000000000000 ) ) ;
#3173=CARTESIAN_POINT ( 'NONE',  ( 20.85000000000000497, 15.03999999999999737, 2.200000000000000178 ) ) ;
#3423=DIRECTION ( 'NONE',  ( -1.000000000000000000, 0.000000000000000000, 0.000000000000000000 ) ) ;
#3677=VECTOR ( 'NONE', #11162, 1000.000000000000000 ) ;
#3788=DIRECTION ( 'NONE',  ( 0.000000000000000000, 0.000000000000000000, 1.000000000000000000 ) ) ;
#3903=CARTESIAN_POINT ( 'NONE',  ( 0.000000000000000000, 15.03999999999999737, 2.200000000000000178 ) ) ;
#3995=CARTESIAN_POINT ( 'NONE',  ( 0.000000000000000000, 15.03999999999999737, 2.200000000000000178 ) ) ;
#4013=LINE ( 'NONE', #474, #5174 ) ;
#4035=EDGE_CURVE ( 'NONE', #19904, #21161, #1838, .T. ) ;
#4092=VERTEX_POINT ( 'NONE', #54 ) ;
#4208=CARTESIAN_POINT ( 'NONE',  ( -23.85000000000000142, 15.03999999999999737, 2.200000000000000178 ) ) ;
#4319=PRODUCT_DEFINITION_CONTEXT ( 'detailed design', #20101, 'design' ) ;
#4351=DIRECTION ( 'NONE',  ( -0.000000000000000000, -0.000000000000000000, -1.000000000000000000 ) ) ;
#4381=VECTOR ( 'NONE', #8189, 1000.000000000000000 ) ;
#4393=( NAMED_UNIT ( * ) SI_UNIT ( $, .STERADIAN. ) SOLID_ANGLE_UNIT ( ) );
#4397=AXIS2_PLACEMENT_3D ( 'NONE', #18513, #7034, #5455 ) ;
#4618=EDGE_LOOP ( 'NONE', ( #14958, #23511, #14689, #11711 ) ) ;
#4647=SHAPE_REPRESENTATION_RELATIONSHIP ( 'NONE' , 'NONE' ,  #9527, #18921 ) ;
#5051=ORIENTED_EDGE ( 'NONE', *, *, #7004, .F. ) ;
#5166=ADVANCED_FACE ( 'NONE', ( #9260 ), #258, .T. ) ;
#5174=VECTOR ( 'NONE', #18548, 1000.000000000000000 ) ;
#5196=AXIS2_PLACEMENT_3D ( 'NONE', #2986, #14073, #14542 ) ;
#5299=AXIS2_PLACEMENT_3D ( 'NONE', #20566, #10785, #16528 ) ;
#5330=ORIENTED_EDGE ( 'NONE', *, *, #15913, .T. ) ;
#5372=DIRECTION ( 'NONE',  ( 0.000000000000000000, 0.000000000000000000, 1.000000000000000000 ) ) ;
#5384=EDGE_LOOP ( 'NONE', ( #13171, #14563, #1331, #17832 ) ) ;
#5410=DIRECTION ( 'NONE',  ( -1.000000000000000000, 0.000000000000000000, 0.000000000000000000 ) ) ;
#5455=DIRECTION ( 'NONE',  ( -1.000000000000000000, 0.000000000000000000, 0.000000000000000000 ) ) ;
#5474=CARTESIAN_POINT ( 'NONE',  ( -23.85000000000000142, 15.03999999999999737, 2.200000000000000178 ) ) ;
#5513=ORIENTED_EDGE ( 'NONE', *, *, #11087, .F. ) ;
#5529=EDGE_LOOP ( 'NONE', ( #16448, #19368, #2118, #5330 ) ) ;
#5657=EDGE_LOOP ( 'NONE', ( #15926, #13650, #23544, #18913 ) ) ;
#5697=EDGE_CURVE ( 'NONE', #16388, #18576, #12717, .T. ) ;
#5766=ADVANCED_FACE ( 'NONE', ( #16263 ), #21768, .T. ) ;
#5770=CARTESIAN_POINT ( 'NONE',  ( 0.000000000000000000, 15.03999999999999737, 2.200000000000000178 ) ) ;
#5816=CARTESIAN_POINT ( 'NONE',  ( -23.85000000000000142, 15.03999999999999737, 0.000000000000000000 ) ) ;
#5848=CARTESIAN_POINT ( 'NONE',  ( -23.85000000000000142, -15.03999999999999737, 2.200000000000000178 ) ) ;
#5913=ORIENTED_EDGE ( 'NONE', *, *, #16180, .T. ) ;
#5958=VECTOR ( 'NONE', #23683, 1000.000000000000000 ) ;
#5978=CARTESIAN_POINT ( 'NONE',  ( 0.000000000000000000, 0.000000000000000000, 0.000000000000000000 ) ) ;
#5993=( NAMED_UNIT ( * ) PLANE_ANGLE_UNIT ( ) SI_UNIT ( $, .RADIAN. ) );
#6176=MECHANICAL_DESIGN_GEOMETRIC_PRESENTATION_REPRESENTATION('',(#20203),#6966);
#6952=DIRECTION ( 'NONE',  ( -0.000000000000000000, 0.000000000000000000, -1.000000000000000000 ) ) ;
#6966=( GEOMETRIC_REPRESENTATION_CONTEXT ( 3 ) GLOBAL_UNCERTAINTY_ASSIGNED_CONTEXT ( ( #3033 ) ) GLOBAL_UNIT_ASSIGNED_CONTEXT ( ( #751, #5993, #637 ) ) REPRESENTATION_CONTEXT ( 'NONE', 'WORKASPACE' ) );
#6981=VERTEX_POINT ( 'NONE', #12495 ) ;
#6999=CARTESIAN_POINT ( 'NONE',  ( 0.000000000000000000, 15.03999999999999737, 0.000000000000000000 ) ) ;
#7004=EDGE_CURVE ( 'NONE', #23803, #16388, #16094, .T. ) ;
#7034=DIRECTION ( 'NONE',  ( -0.000000000000000000, -0.000000000000000000, -1.000000000000000000 ) ) ;
#7108=DIRECTION ( 'NONE',  ( 0.000000000000000000, 0.000000000000000000, 1.000000000000000000 ) ) ;
#7202=EDGE_LOOP ( 'NONE', ( #2302, #12834, #13885, #19772 ) ) ;
#7397=ADVANCED_FACE ( 'NONE', ( #23374 ), #3098, .F. ) ;
#7423=DIRECTION ( 'NONE',  ( 0.000000000000000000, 0.000000000000000000, 1.000000000000000000 ) ) ;
#7428=AXIS2_PLACEMENT_3D ( 'NONE', #3168, #5372, #12797 ) ;
#7563=ADVANCED_FACE ( 'NONE', ( #18813 ), #165, .T. ) ;
#7588=DIRECTION ( 'NONE',  ( 1.000000000000000000, 0.000000000000000000, 0.000000000000000000 ) ) ;
#7606=PRODUCT_CONTEXT ( 'NONE', #11474, 'mechanical' ) ;
#7663=CARTESIAN_POINT ( 'NONE',  ( 20.85000000000000497, 15.03999999999999737, 2.200000000000000178 ) ) ;
#7942=EDGE_CURVE ( 'NONE', #19904, #23803, #17771, .T. ) ;
#7947=DIRECTION ( 'NONE',  ( -0.000000000000000000, -0.000000000000000000, -1.000000000000000000 ) ) ;
#7949=ADVANCED_FACE ( 'NONE', ( #12615, #16170 ), #1179, .F. ) ;
#8005=AXIS2_PLACEMENT_3D ( 'NONE', #5978, #22344, #13412 ) ;
#8010=VECTOR ( 'NONE', #18111, 1000.000000000000000 ) ;
#8175=ORIENTED_EDGE ( 'NONE', *, *, #13668, .T. ) ;
#8189=DIRECTION ( 'NONE',  ( 0.000000000000000000, -1.000000000000000000, 0.000000000000000000 ) ) ;
#8328=LINE ( 'NONE', #17735, #4381 ) ;
#8381=EDGE_CURVE ( 'NONE', #9521, #6981, #4013, .T. ) ;
#8387=VECTOR ( 'NONE', #21319, 1000.000000000000000 ) ;
#8400=AXIS2_PLACEMENT_3D ( 'NONE', #3903, #7423, #369 ) ;
#8529=CARTESIAN_POINT ( 'NONE',  ( 23.85000000000000142, 15.03999999999999737, 2.200000000000000178 ) ) ;
#8575=DIRECTION ( 'NONE',  ( -0.000000000000000000, -0.000000000000000000, -1.000000000000000000 ) ) ;
#8603=ORIENTED_EDGE ( 'NONE', *, *, #11375, .T. ) ;
#8687=VECTOR ( 'NONE', #22316, 1000.000000000000000 ) ;
#8719=CARTESIAN_POINT ( 'NONE',  ( 20.85000000000000497, 15.03999999999999737, 2.200000000000000178 ) ) ;
#8818=AXIS2_PLACEMENT_3D ( 'NONE', #6999, #18124, #21538 ) ;
#8824=LINE ( 'NONE', #20060, #8010 ) ;
#8931=PLANE ( 'NONE',  #2566 ) ;
#9034=ORIENTED_EDGE ( 'NONE', *, *, #11087, .T. ) ;
#9057=VECTOR ( 'NONE', #14944, 1000.000000000000000 ) ;
#9224=CARTESIAN_POINT ( 'NONE',  ( -23.85000000000000142, 15.03999999999999737, 0.000000000000000000 ) ) ;
#9260=FACE_OUTER_BOUND ( 'NONE', #4618, .T. ) ;
#9300=CARTESIAN_POINT ( 'NONE',  ( 0.000000000000000000, 15.03999999999999737, 2.200000000000000178 ) ) ;
#9355=PRODUCT ( 'Housing Seal', 'Housing Seal', '', ( #7606 ) ) ;
#9394=ADVANCED_FACE ( 'NONE', ( #23766 ), #1456, .T. ) ;
#9460=EDGE_CURVE ( 'NONE', #2565, #21660, #24002, .T. ) ;
#9502=VECTOR ( 'NONE', #13373, 1000.000000000000000 ) ;
#9521=VERTEX_POINT ( 'NONE', #20225 ) ;
#9527=SHAPE_REPRESENTATION ( 'Housing Seal', ( #8005 ), #12698 ) ;
#9541=ORIENTED_EDGE ( 'NONE', *, *, #22268, .F. ) ;
#9558=CIRCLE ( 'NONE', #5299, 20.85000000000000497 ) ;
#9628=EDGE_CURVE ( 'NONE', #21161, #16388, #13613, .T. ) ;
#10018=ORIENTED_EDGE ( 'NONE', *, *, #8381, .F. ) ;
#10130=ORIENTED_EDGE ( 'NONE', *, *, #20817, .T. ) ;
#10310=AXIS2_PLACEMENT_3D ( 'NONE', #7663, #20263, #3788 ) ;
#10413=CARTESIAN_POINT ( 'NONE',  ( -20.85000000000000497, 15.03999999999999915, 0.000000000000000000 ) ) ;
#10434=LINE ( 'NONE', #21434, #8387 ) ;
#10616=VECTOR ( 'NONE', #19732, 1000.000000000000000 ) ;
#10753=ORIENTED_EDGE ( 'NONE', *, *, #7942, .F. ) ;
#10780=DIRECTION ( 'NONE',  ( -0.000000000000000000, 1.000000000000000000, -0.000000000000000000 ) ) ;
#10785=DIRECTION ( 'NONE',  ( 0.000000000000000000, 0.000000000000000000, 1.000000000000000000 ) ) ;
#10981=DIRECTION ( 'NONE',  ( -0.000000000000000000, -0.000000000000000000, -1.000000000000000000 ) ) ;
#11033=CARTESIAN_POINT ( 'NONE',  ( 0.000000000000000000, -15.03999999999999737, 2.200000000000000178 ) ) ;
#11060=CARTESIAN_POINT ( 'NONE',  ( -20.85000000000000497, -15.03999999999999737, 2.200000000000000178 ) ) ;
#11087=EDGE_CURVE ( 'NONE', #9521, #14785, #11130, .T. ) ;
#11130=LINE ( 'NONE', #23976, #14473 ) ;
#11162=DIRECTION ( 'NONE',  ( 0.000000000000000000, -1.000000000000000000, 0.000000000000000000 ) ) ;
#11174=ORIENTED_EDGE ( 'NONE', *, *, #18875, .T. ) ;
#11210=EDGE_LOOP ( 'NONE', ( #13247, #13184, #10130, #5913 ) ) ;
#11278=ORIENTED_EDGE ( 'NONE', *, *, #14374, .T. ) ;
#11305=ORIENTED_EDGE ( 'NONE', *, *, #14374, .F. ) ;
#11375=EDGE_CURVE ( 'NONE', #17477, #530, #8328, .T. ) ;
#11474=APPLICATION_CONTEXT ( 'automotive_design' ) ;
#11600=ORIENTED_EDGE ( 'NONE', *, *, #11375, .F. ) ;
#11707=EDGE_CURVE ( 'NONE', #17720, #23803, #21480, .T. ) ;
#11711=ORIENTED_EDGE ( 'NONE', *, *, #7942, .T. ) ;
#12472=CARTESIAN_POINT ( 'NONE',  ( -20.85000000000000497, -15.03999999999999737, 0.000000000000000000 ) ) ;
#12495=CARTESIAN_POINT ( 'NONE',  ( 23.85000000000000142, -15.03999999999999737, 0.000000000000000000 ) ) ;
#12615=FACE_OUTER_BOUND ( 'NONE', #19471, .T. ) ;
#12698=( GEOMETRIC_REPRESENTATION_CONTEXT ( 3 ) GLOBAL_UNCERTAINTY_ASSIGNED_CONTEXT ( ( #13256 ) ) GLOBAL_UNIT_ASSIGNED_CONTEXT ( ( #21358, #2681, #4393 ) ) REPRESENTATION_CONTEXT ( 'NONE', 'WORKASPACE' ) );
#12717=LINE ( 'NONE', #10413, #20786 ) ;
#12721=FACE_OUTER_BOUND ( 'NONE', #19038, .T. ) ;
#12725=AXIS2_PLACEMENT_3D ( 'NONE', #9300, #16744, #7588 ) ;
#12797=DIRECTION ( 'NONE',  ( -1.000000000000000000, 0.000000000000000000, 0.000000000000000000 ) ) ;
#12834=ORIENTED_EDGE ( 'NONE', *, *, #4035, .F. ) ;
#13021=CIRCLE ( 'NONE', #15764, 23.85000000000000142 ) ;
#13026=AXIS2_PLACEMENT_3D ( 'NONE', #11033, #211, #1907 ) ;
#13061=ORIENTED_EDGE ( 'NONE', *, *, #8381, .T. ) ;
#13171=ORIENTED_EDGE ( 'NONE', *, *, #22268, .T. ) ;
#13184=ORIENTED_EDGE ( 'NONE', *, *, #15913, .F. ) ;
#13207=EDGE_CURVE ( 'NONE', #530, #21660, #18772, .T. ) ;
#13223=ORIENTED_EDGE ( 'NONE', *, *, #18875, .F. ) ;
#13247=ORIENTED_EDGE ( 'NONE', *, *, #13290, .F. ) ;
#13256=UNCERTAINTY_MEASURE_WITH_UNIT (LENGTH_MEASURE( 1.000000000000000082E-05 ), #21358, 'distance_accuracy_value', 'NONE');
#13264=CARTESIAN_POINT ( 'NONE',  ( -20.85000000000000497, 15.03999999999999915, 2.200000000000000178 ) ) ;
#13290=EDGE_CURVE ( 'NONE', #18576, #17720, #9558, .T. ) ;
#13343=AXIS2_PLACEMENT_3D ( 'NONE', #5474, #19779, #6952 ) ;
#13373=DIRECTION ( 'NONE',  ( -0.000000000000000000, 1.000000000000000000, -0.000000000000000000 ) ) ;
#13412=DIRECTION ( 'NONE',  ( 1.000000000000000000, 0.000000000000000000, 0.000000000000000000 ) ) ;
#13613=LINE ( 'NONE', #18741, #21579 ) ;
#13628=ORIENTED_EDGE ( 'NONE', *, *, #13207, .T. ) ;
#13650=ORIENTED_EDGE ( 'NONE', *, *, #5697, .T. ) ;
#13668=EDGE_CURVE ( 'NONE', #17477, #2565, #8824, .T. ) ;
#13711=ADVANCED_FACE ( 'NONE', ( #12721 ), #8931, .F. ) ;
#13774=PRODUCT_DEFINITION ( 'UNKNOWN', '', #2202, #4319 ) ;
#13885=ORIENTED_EDGE ( 'NONE', *, *, #2492, .F. ) ;
#14005=CARTESIAN_POINT ( 'NONE',  ( 20.85000000000000497, -15.04000000000000270, 2.200000000000000178 ) ) ;
#14073=DIRECTION ( 'NONE',  ( 1.000000000000000000, 0.000000000000000000, -0.000000000000000000 ) ) ;
#14374=EDGE_CURVE ( 'NONE', #6981, #19122, #10434, .T. ) ;
#14473=VECTOR ( 'NONE', #10780, 1000.000000000000000 ) ;
#14542=DIRECTION ( 'NONE',  ( -0.000000000000000000, 0.000000000000000000, -1.000000000000000000 ) ) ;
#14563=ORIENTED_EDGE ( 'NONE', *, *, #13668, .F. ) ;
#14605=ORIENTED_EDGE ( 'NONE', *, *, #9460, .T. ) ;
#14625=LINE ( 'NONE', #11060, #8687 ) ;
#14637=CARTESIAN_POINT ( 'NONE',  ( 0.000000000000000000, -15.03999999999999737, 2.200000000000000178 ) ) ;
#14684=ORIENTED_EDGE ( 'NONE', *, *, #13207, .F. ) ;
#14689=ORIENTED_EDGE ( 'NONE', *, *, #2492, .T. ) ;
#14706=SHAPE_DEFINITION_REPRESENTATION ( #3024, #9527 ) ;
#14785=VERTEX_POINT ( 'NONE', #8529 ) ;
#14897=DIRECTION ( 'NONE',  ( -1.000000000000000000, 0.000000000000000000, 0.000000000000000000 ) ) ;
#14932=ORIENTED_EDGE ( 'NONE', *, *, #2348, .F. ) ;
#14944=DIRECTION ( 'NONE',  ( 0.000000000000000000, -1.000000000000000000, 0.000000000000000000 ) ) ;
#14958=ORIENTED_EDGE ( 'NONE', *, *, #11707, .F. ) ;
#14992=FACE_BOUND ( 'NONE', #7202, .T. ) ;
#15054=ADVANCED_FACE ( 'NONE', ( #22225, #14992 ), #18673, .T. ) ;
#15157=EDGE_LOOP ( 'NONE', ( #14605, #14684, #11600, #8175 ) ) ;
#15180=LINE ( 'NONE', #20466, #9502 ) ;
#15257=DIRECTION ( 'NONE',  ( -1.000000000000000000, 0.000000000000000000, 0.000000000000000000 ) ) ;
#15542=CARTESIAN_POINT ( 'NONE',  ( 23.85000000000000142, 15.03999999999999737, 2.200000000000000178 ) ) ;
#15618=CIRCLE ( 'NONE', #7428, 23.85000000000000142 ) ;
#15764=AXIS2_PLACEMENT_3D ( 'NONE', #14637, #22108, #3423 ) ;
#15784=CARTESIAN_POINT ( 'NONE',  ( 20.85000000000000497, -15.04000000000000270, 0.000000000000000000 ) ) ;
#15913=EDGE_CURVE ( 'NONE', #21353, #18576, #14625, .T. ) ;
#15926=ORIENTED_EDGE ( 'NONE', *, *, #7004, .T. ) ;
#15977=CARTESIAN_POINT ( 'NONE',  ( 20.85000000000000497, 15.03999999999999737, 0.000000000000000000 ) ) ;
#16031=CARTESIAN_POINT ( 'NONE',  ( 0.000000000000000000, 15.03999999999999737, 2.200000000000000178 ) ) ;
#16040=DIRECTION ( 'NONE',  ( 0.000000000000000000, 0.000000000000000000, 1.000000000000000000 ) ) ;
#16094=CIRCLE ( 'NONE', #19216, 20.85000000000000497 ) ;
#16170=FACE_BOUND ( 'NONE', #5657, .T. ) ;
#16180=EDGE_CURVE ( 'NONE', #4092, #17720, #957, .T. ) ;
#16263=FACE_OUTER_BOUND ( 'NONE', #5529, .T. ) ;
#16388=VERTEX_POINT ( 'NONE', #19361 ) ;
#16448=ORIENTED_EDGE ( 'NONE', *, *, #5697, .F. ) ;
#16449=AXIS2_PLACEMENT_3D ( 'NONE', #5770, #10981, #14897 ) ;
#16527=DIRECTION ( 'NONE',  ( 0.000000000000000000, 0.000000000000000000, 1.000000000000000000 ) ) ;
#16528=DIRECTION ( 'NONE',  ( -1.000000000000000000, 0.000000000000000000, 0.000000000000000000 ) ) ;
#16698=CLOSED_SHELL ( 'NONE', ( #15054, #7949, #7563, #1202, #9394, #13711, #1438, #5766, #7397, #5166 ) ) ;
#16744=DIRECTION ( 'NONE',  ( 0.000000000000000000, 0.000000000000000000, 1.000000000000000000 ) ) ;
#17033=LINE ( 'NONE', #18747, #3677 ) ;
#17093=CARTESIAN_POINT ( 'NONE',  ( 20.85000000000000497, 15.03999999999999737, 0.000000000000000000 ) ) ;
#17315=CARTESIAN_POINT ( 'NONE',  ( -23.85000000000000142, -15.03999999999999737, 2.200000000000000178 ) ) ;
#17477=VERTEX_POINT ( 'NONE', #4208 ) ;
#17720=VERTEX_POINT ( 'NONE', #15784 ) ;
#17735=CARTESIAN_POINT ( 'NONE',  ( -23.85000000000000142, 15.03999999999999737, 2.200000000000000178 ) ) ;
#17771=LINE ( 'NONE', #8719, #10616 ) ;
#17832=ORIENTED_EDGE ( 'NONE', *, *, #1289, .T. ) ;
#17921=CARTESIAN_POINT ( 'NONE',  ( 23.85000000000000142, 15.03999999999999737, 0.000000000000000000 ) ) ;
#17984=DIRECTION ( 'NONE',  ( -1.000000000000000000, 0.000000000000000000, 0.000000000000000000 ) ) ;
#17995=VECTOR ( 'NONE', #20823, 1000.000000000000000 ) ;
#18111=DIRECTION ( 'NONE',  ( -0.000000000000000000, -0.000000000000000000, -1.000000000000000000 ) ) ;
#18124=DIRECTION ( 'NONE',  ( 0.000000000000000000, 0.000000000000000000, 1.000000000000000000 ) ) ;
#18175=CIRCLE ( 'NONE', #22838, 23.85000000000000142 ) ;
#18229=CARTESIAN_POINT ( 'NONE',  ( 0.000000000000000000, -15.03999999999999737, 2.200000000000000178 ) ) ;
#18513=CARTESIAN_POINT ( 'NONE',  ( 0.000000000000000000, -15.03999999999999737, 2.200000000000000178 ) ) ;
#18548=DIRECTION ( 'NONE',  ( -0.000000000000000000, -0.000000000000000000, -1.000000000000000000 ) ) ;
#18569=CARTESIAN_POINT ( 'NONE',  ( -23.85000000000000142, -15.03999999999999737, 0.000000000000000000 ) ) ;
#18576=VERTEX_POINT ( 'NONE', #12472 ) ;
#18673=PLANE ( 'NONE',  #8400 ) ;
#18741=CARTESIAN_POINT ( 'NONE',  ( -20.85000000000000497, 15.03999999999999915, 2.200000000000000178 ) ) ;
#18747=CARTESIAN_POINT ( 'NONE',  ( -20.85000000000000497, 15.03999999999999915, 2.200000000000000178 ) ) ;
#18772=LINE ( 'NONE', #5848, #23618 ) ;
#18813=FACE_OUTER_BOUND ( 'NONE', #5384, .T. ) ;
#18875=EDGE_CURVE ( 'NONE', #21660, #6981, #15618, .T. ) ;
#18913=ORIENTED_EDGE ( 'NONE', *, *, #11707, .T. ) ;
#18921=ADVANCED_BREP_SHAPE_REPRESENTATION ( '', ( #2159, #8005 ), #12698 ) ;
#18932=ORIENTED_EDGE ( 'NONE', *, *, #2348, .T. ) ;
#19038=EDGE_LOOP ( 'NONE', ( #11278, #20268, #5513, #13061 ) ) ;
#19106=LINE ( 'NONE', #15542, #17995 ) ;
#19122=VERTEX_POINT ( 'NONE', #17921 ) ;
#19216=AXIS2_PLACEMENT_3D ( 'NONE', #1303, #16527, #23981 ) ;
#19246=VECTOR ( 'NONE', #21452, 1000.000000000000000 ) ;
#19361=CARTESIAN_POINT ( 'NONE',  ( -20.85000000000000497, 15.03999999999999915, 0.000000000000000000 ) ) ;
#19368=ORIENTED_EDGE ( 'NONE', *, *, #9628, .F. ) ;
#19406=FACE_OUTER_BOUND ( 'NONE', #15157, .T. ) ;
#19471=EDGE_LOOP ( 'NONE', ( #9541, #11305, #13223, #19804 ) ) ;
#19732=DIRECTION ( 'NONE',  ( -0.000000000000000000, -0.000000000000000000, -1.000000000000000000 ) ) ;
#19772=ORIENTED_EDGE ( 'NONE', *, *, #20817, .F. ) ;
#19779=DIRECTION ( 'NONE',  ( 1.000000000000000000, 0.000000000000000000, -0.000000000000000000 ) ) ;
#19804=ORIENTED_EDGE ( 'NONE', *, *, #9460, .F. ) ;
#19840=CYLINDRICAL_SURFACE ( 'NONE', #1679, 20.85000000000000497 ) ;
#19904=VERTEX_POINT ( 'NONE', #3173 ) ;
#19945=FACE_OUTER_BOUND ( 'NONE', #364, .T. ) ;
#20060=CARTESIAN_POINT ( 'NONE',  ( -23.85000000000000142, 15.03999999999999737, 2.200000000000000178 ) ) ;
#20081=CARTESIAN_POINT ( 'NONE',  ( 0.000000000000000000, 15.03999999999999737, 0.000000000000000000 ) ) ;
#20101=APPLICATION_CONTEXT ( 'automotive_design' ) ;
#20203=STYLED_ITEM('',(#24162),#2159);
#20225=CARTESIAN_POINT ( 'NONE',  ( 23.85000000000000142, -15.03999999999999737, 2.200000000000000178 ) ) ;
#20263=DIRECTION ( 'NONE',  ( -1.000000000000000000, 0.000000000000000000, 0.000000000000000000 ) ) ;
#20268=ORIENTED_EDGE ( 'NONE', *, *, #1289, .F. ) ;
#20466=CARTESIAN_POINT ( 'NONE',  ( 20.85000000000000497, 15.03999999999999737, 2.200000000000000178 ) ) ;
#20483=DIRECTION ( 'NONE',  ( 0.000000000000000000, 0.000000000000000000, 1.000000000000000000 ) ) ;
#20566=CARTESIAN_POINT ( 'NONE',  ( 0.000000000000000000, -15.03999999999999737, 0.000000000000000000 ) ) ;
#20786=VECTOR ( 'NONE', #21523, 1000.000000000000000 ) ;
#20817=EDGE_CURVE ( 'NONE', #21353, #4092, #23579, .T. ) ;
#20823=DIRECTION ( 'NONE',  ( -0.000000000000000000, -0.000000000000000000, -1.000000000000000000 ) ) ;
#20935=CARTESIAN_POINT ( 'NONE',  ( -20.85000000000000497, -15.03999999999999737, 2.200000000000000178 ) ) ;
#21161=VERTEX_POINT ( 'NONE', #13264 ) ;
#21319=DIRECTION ( 'NONE',  ( -0.000000000000000000, 1.000000000000000000, -0.000000000000000000 ) ) ;
#21353=VERTEX_POINT ( 'NONE', #20935 ) ;
#21358=( LENGTH_UNIT ( ) NAMED_UNIT ( * ) SI_UNIT ( .MILLI., .METRE. ) );
#21434=CARTESIAN_POINT ( 'NONE',  ( 23.85000000000000142, 15.03999999999999737, 0.000000000000000000 ) ) ;
#21452=DIRECTION ( 'NONE',  ( -0.000000000000000000, -0.000000000000000000, -1.000000000000000000 ) ) ;
#21480=LINE ( 'NONE', #15977, #5958 ) ;
#21523=DIRECTION ( 'NONE',  ( 0.000000000000000000, -1.000000000000000000, 0.000000000000000000 ) ) ;
#21538=DIRECTION ( 'NONE',  ( 1.000000000000000000, 0.000000000000000000, 0.000000000000000000 ) ) ;
#21579=VECTOR ( 'NONE', #4351, 1000.000000000000000 ) ;
#21660=VERTEX_POINT ( 'NONE', #18569 ) ;
#21768=PLANE ( 'NONE',  #5196 ) ;
#22070=EDGE_CURVE ( 'NONE', #14785, #17477, #18175, .T. ) ;
#22108=DIRECTION ( 'NONE',  ( 0.000000000000000000, 0.000000000000000000, 1.000000000000000000 ) ) ;
#22216=DIRECTION ( 'NONE',  ( -0.000000000000000000, -0.000000000000000000, -1.000000000000000000 ) ) ;
#22225=FACE_OUTER_BOUND ( 'NONE', #22682, .T. ) ;
#22268=EDGE_CURVE ( 'NONE', #19122, #2565, #2985, .T. ) ;
#22316=DIRECTION ( 'NONE',  ( -0.000000000000000000, -0.000000000000000000, -1.000000000000000000 ) ) ;
#22344=DIRECTION ( 'NONE',  ( 0.000000000000000000, 0.000000000000000000, 1.000000000000000000 ) ) ;
#22682=EDGE_LOOP ( 'NONE', ( #2613, #8603, #18932, #9034 ) ) ;
#22838=AXIS2_PLACEMENT_3D ( 'NONE', #3995, #20483, #1825 ) ;
#23001=EDGE_LOOP ( 'NONE', ( #11174, #10018, #14932, #13628 ) ) ;
#23374=FACE_OUTER_BOUND ( 'NONE', #11210, .T. ) ;
#23502=DIRECTION ( 'NONE',  ( 1.000000000000000000, 0.000000000000000000, -0.000000000000000000 ) ) ;
#23511=ORIENTED_EDGE ( 'NONE', *, *, #16180, .F. ) ;
#23544=ORIENTED_EDGE ( 'NONE', *, *, #13290, .T. ) ;
#23579=CIRCLE ( 'NONE', #13026, 20.85000000000000497 ) ;
#23618=VECTOR ( 'NONE', #22216, 1000.000000000000000 ) ;
#23678=ORIENTED_EDGE ( 'NONE', *, *, #9628, .T. ) ;
#23683=DIRECTION ( 'NONE',  ( -0.000000000000000000, 1.000000000000000000, -0.000000000000000000 ) ) ;
#23766=FACE_OUTER_BOUND ( 'NONE', #23001, .T. ) ;
#23803=VERTEX_POINT ( 'NONE', #17093 ) ;
#23828=CARTESIAN_POINT ( 'NONE',  ( 23.85000000000000142, 15.03999999999999737, 2.200000000000000178 ) ) ;
#23976=CARTESIAN_POINT ( 'NONE',  ( 23.85000000000000142, 15.03999999999999737, 2.200000000000000178 ) ) ;
#23981=DIRECTION ( 'NONE',  ( 1.000000000000000000, 0.000000000000000000, 0.000000000000000000 ) ) ;
#24002=LINE ( 'NONE', #9224, #9057 ) ;
#24156=COLOUR_RGB('Black',0.12,0.14,0.17);
#24157=FILL_AREA_STYLE_COLOUR('',#24156);
#24158=FILL_AREA_STYLE('',(#24157));
#24159=SURFACE_STYLE_FILL_AREA(#24158);
#24160=SURFACE_SIDE_STYLE('',(#24159));
#24161=SURFACE_STYLE_USAGE(.BOTH.,#24160);
#24162=PRESENTATION_STYLE_ASSIGNMENT((#24161));
ENDSEC;
END-ISO-10303-21;
